ISO-10303-21;
HEADER;
/* Generated by software containing ST-Developer
 * from STEP Tools, Inc. (www.steptools.com) 
 */

FILE_DESCRIPTION(
/* description */ (''),
/* implementation_level */ '2;1');

FILE_NAME(
/* name */ 'Screw_01.step',
/* time_stamp */ '2026-10-04T23:23:09-07:00',
/* author */ (''),
/* organization */ (''),
/* preprocessor_version */ 'ST-DEVELOPER v20.2',
/* originating_system */ 'Autodesk Translation Framework v15.15.0.0',
/* authorisation */ '');

FILE_SCHEMA (('AUTOMOTIVE_DESIGN { 1 0 10303 214 3 1 1 }'));
ENDSEC;

DATA;
#10=MECHANICAL_DESIGN_GEOMETRIC_PRESENTATION_REPRESENTATION('',(#68,#69),#2676);
#44=SPHERICAL_SURFACE('',#1670,1.);
#51=SHAPE_REPRESENTATION_RELATIONSHIP('SRR','None',#2710,#59);
#59=ADVANCED_BREP_SHAPE_REPRESENTATION('',(#79,#80),#2670);
#68=STYLED_ITEM('',(#2757),#79);
#69=STYLED_ITEM('',(#2757),#80);
#79=MANIFOLD_SOLID_BREP('Body1',#1479);
#80=MANIFOLD_SOLID_BREP('Body1',#1480);
#96=CYLINDRICAL_SURFACE('',#1643,1.);
#97=CYLINDRICAL_SURFACE('',#1647,2.);
#98=CYLINDRICAL_SURFACE('',#1655,1.);
#99=CYLINDRICAL_SURFACE('',#1659,1.);
#100=CYLINDRICAL_SURFACE('',#1663,2.);
#119=FACE_BOUND('',#329,.T.);
#120=FACE_BOUND('',#334,.T.);
#121=FACE_BOUND('',#337,.T.);
#122=FACE_BOUND('',#342,.T.);
#123=FACE_BOUND('',#346,.T.);
#151=PLANE('',#1640);
#152=PLANE('',#1649);
#153=PLANE('',#1652);
#154=PLANE('',#1657);
#155=PLANE('',#1661);
#156=PLANE('',#1667);
#220=FACE_OUTER_BOUND('',#328,.T.);
#221=FACE_OUTER_BOUND('',#330,.T.);
#222=FACE_OUTER_BOUND('',#331,.T.);
#223=FACE_OUTER_BOUND('',#332,.T.);
#224=FACE_OUTER_BOUND('',#333,.T.);
#225=FACE_OUTER_BOUND('',#335,.T.);
#226=FACE_OUTER_BOUND('',#336,.T.);
#227=FACE_OUTER_BOUND('',#338,.T.);
#228=FACE_OUTER_BOUND('',#339,.T.);
#229=FACE_OUTER_BOUND('',#340,.T.);
#230=FACE_OUTER_BOUND('',#341,.T.);
#231=FACE_OUTER_BOUND('',#343,.T.);
#232=FACE_OUTER_BOUND('',#344,.T.);
#233=FACE_OUTER_BOUND('',#345,.T.);
#234=FACE_OUTER_BOUND('',#347,.T.);
#235=FACE_OUTER_BOUND('',#348,.T.);
#328=EDGE_LOOP('',(#1114));
#329=EDGE_LOOP('',(#1115));
#330=EDGE_LOOP('',(#1116,#1117,#1118,#1119));
#331=EDGE_LOOP('',(#1120,#1121,#1122,#1123));
#332=EDGE_LOOP('',(#1124,#1125,#1126,#1127));
#333=EDGE_LOOP('',(#1128));
#334=EDGE_LOOP('',(#1129));
#335=EDGE_LOOP('',(#1130,#1131,#1132,#1133));
#336=EDGE_LOOP('',(#1134));
#337=EDGE_LOOP('',(#1135));
#338=EDGE_LOOP('',(#1136,#1137,#1138,#1139));
#339=EDGE_LOOP('',(#1140));
#340=EDGE_LOOP('',(#1141,#1142,#1143,#1144));
#341=EDGE_LOOP('',(#1145));
#342=EDGE_LOOP('',(#1146));
#343=EDGE_LOOP('',(#1147,#1148,#1149,#1150));
#344=EDGE_LOOP('',(#1151,#1152,#1153,#1154));
#345=EDGE_LOOP('',(#1155));
#346=EDGE_LOOP('',(#1156));
#347=EDGE_LOOP('',(#1157,#1158,#1159,#1160));
#348=EDGE_LOOP('',(#1161,#1162,#1163));
#440=LINE('',#2384,#550);
#441=LINE('',#2387,#551);
#442=LINE('',#2391,#552);
#443=LINE('',#2397,#553);
#444=LINE('',#2405,#554);
#445=LINE('',#2413,#555);
#446=LINE('',#2420,#556);
#447=LINE('',#2423,#557);
#448=LINE('',#2429,#558);
#550=VECTOR('',#1931,1.);
#551=VECTOR('',#1934,1.1);
#552=VECTOR('',#1939,2.);
#553=VECTOR('',#1948,1.9);
#554=VECTOR('',#1957,1.);
#555=VECTOR('',#1968,1.);
#556=VECTOR('',#1977,2.);
#557=VECTOR('',#1980,1.9);
#558=VECTOR('',#1989,1.1);
#656=CIRCLE('',#1641,2.);
#657=CIRCLE('',#1642,1.);
#658=CIRCLE('',#1644,1.);
#659=CIRCLE('',#1646,1.2);
#660=CIRCLE('',#1648,2.);
#661=CIRCLE('',#1650,1.8);
#662=CIRCLE('',#1653,1.);
#663=CIRCLE('',#1654,0.866025403784439);
#664=CIRCLE('',#1656,1.);
#665=CIRCLE('',#1658,1.);
#666=CIRCLE('',#1660,1.);
#667=CIRCLE('',#1662,2.);
#668=CIRCLE('',#1664,2.);
#669=CIRCLE('',#1666,1.8);
#670=CIRCLE('',#1668,1.2);
#671=CIRCLE('',#1671,1.);
#737=VERTEX_POINT('',#2377);
#738=VERTEX_POINT('',#2379);
#739=VERTEX_POINT('',#2382);
#740=VERTEX_POINT('',#2386);
#741=VERTEX_POINT('',#2390);
#742=VERTEX_POINT('',#2394);
#743=VERTEX_POINT('',#2399);
#744=VERTEX_POINT('',#2401);
#745=VERTEX_POINT('',#2404);
#746=VERTEX_POINT('',#2408);
#747=VERTEX_POINT('',#2411);
#748=VERTEX_POINT('',#2415);
#749=VERTEX_POINT('',#2418);
#750=VERTEX_POINT('',#2422);
#751=VERTEX_POINT('',#2426);
#752=VERTEX_POINT('',#2431);
#875=EDGE_CURVE('',#737,#737,#656,.T.);
#876=EDGE_CURVE('',#738,#738,#657,.T.);
#877=EDGE_CURVE('',#739,#739,#658,.T.);
#878=EDGE_CURVE('',#739,#738,#440,.T.);
#879=EDGE_CURVE('',#739,#740,#441,.T.);
#880=EDGE_CURVE('',#740,#740,#659,.T.);
#881=EDGE_CURVE('',#737,#741,#442,.T.);
#882=EDGE_CURVE('',#741,#741,#660,.T.);
#883=EDGE_CURVE('',#742,#742,#661,.T.);
#884=EDGE_CURVE('',#741,#742,#443,.T.);
#885=EDGE_CURVE('',#743,#743,#662,.T.);
#886=EDGE_CURVE('',#744,#744,#663,.T.);
#887=EDGE_CURVE('',#743,#745,#444,.T.);
#888=EDGE_CURVE('',#745,#745,#664,.T.);
#889=EDGE_CURVE('',#746,#746,#665,.T.);
#890=EDGE_CURVE('',#747,#747,#666,.T.);
#891=EDGE_CURVE('',#747,#746,#445,.T.);
#892=EDGE_CURVE('',#748,#748,#667,.T.);
#893=EDGE_CURVE('',#749,#749,#668,.T.);
#894=EDGE_CURVE('',#749,#748,#446,.T.);
#895=EDGE_CURVE('',#749,#750,#447,.T.);
#896=EDGE_CURVE('',#750,#750,#669,.T.);
#897=EDGE_CURVE('',#751,#751,#670,.T.);
#898=EDGE_CURVE('',#745,#751,#448,.T.);
#899=EDGE_CURVE('',#744,#752,#671,.T.);
#1114=ORIENTED_EDGE('',*,*,#875,.T.);
#1115=ORIENTED_EDGE('',*,*,#876,.T.);
#1116=ORIENTED_EDGE('',*,*,#877,.F.);
#1117=ORIENTED_EDGE('',*,*,#878,.T.);
#1118=ORIENTED_EDGE('',*,*,#876,.F.);
#1119=ORIENTED_EDGE('',*,*,#878,.F.);
#1120=ORIENTED_EDGE('',*,*,#877,.T.);
#1121=ORIENTED_EDGE('',*,*,#879,.T.);
#1122=ORIENTED_EDGE('',*,*,#880,.T.);
#1123=ORIENTED_EDGE('',*,*,#879,.F.);
#1124=ORIENTED_EDGE('',*,*,#875,.F.);
#1125=ORIENTED_EDGE('',*,*,#881,.T.);
#1126=ORIENTED_EDGE('',*,*,#882,.F.);
#1127=ORIENTED_EDGE('',*,*,#881,.F.);
#1128=ORIENTED_EDGE('',*,*,#883,.F.);
#1129=ORIENTED_EDGE('',*,*,#880,.F.);
#1130=ORIENTED_EDGE('',*,*,#882,.T.);
#1131=ORIENTED_EDGE('',*,*,#884,.T.);
#1132=ORIENTED_EDGE('',*,*,#883,.T.);
#1133=ORIENTED_EDGE('',*,*,#884,.F.);
#1134=ORIENTED_EDGE('',*,*,#885,.T.);
#1135=ORIENTED_EDGE('',*,*,#886,.T.);
#1136=ORIENTED_EDGE('',*,*,#885,.F.);
#1137=ORIENTED_EDGE('',*,*,#887,.T.);
#1138=ORIENTED_EDGE('',*,*,#888,.T.);
#1139=ORIENTED_EDGE('',*,*,#887,.F.);
#1140=ORIENTED_EDGE('',*,*,#889,.T.);
#1141=ORIENTED_EDGE('',*,*,#890,.T.);
#1142=ORIENTED_EDGE('',*,*,#891,.T.);
#1143=ORIENTED_EDGE('',*,*,#889,.F.);
#1144=ORIENTED_EDGE('',*,*,#891,.F.);
#1145=ORIENTED_EDGE('',*,*,#892,.F.);
#1146=ORIENTED_EDGE('',*,*,#890,.F.);
#1147=ORIENTED_EDGE('',*,*,#893,.F.);
#1148=ORIENTED_EDGE('',*,*,#894,.T.);
#1149=ORIENTED_EDGE('',*,*,#892,.T.);
#1150=ORIENTED_EDGE('',*,*,#894,.F.);
#1151=ORIENTED_EDGE('',*,*,#893,.T.);
#1152=ORIENTED_EDGE('',*,*,#895,.T.);
#1153=ORIENTED_EDGE('',*,*,#896,.T.);
#1154=ORIENTED_EDGE('',*,*,#895,.F.);
#1155=ORIENTED_EDGE('',*,*,#896,.F.);
#1156=ORIENTED_EDGE('',*,*,#897,.F.);
#1157=ORIENTED_EDGE('',*,*,#888,.F.);
#1158=ORIENTED_EDGE('',*,*,#898,.T.);
#1159=ORIENTED_EDGE('',*,*,#897,.T.);
#1160=ORIENTED_EDGE('',*,*,#898,.F.);
#1161=ORIENTED_EDGE('',*,*,#886,.F.);
#1162=ORIENTED_EDGE('',*,*,#899,.T.);
#1163=ORIENTED_EDGE('',*,*,#899,.F.);
#1367=CONICAL_SURFACE('',#1645,1.1,0.785398163397448);
#1368=CONICAL_SURFACE('',#1651,1.9,0.785398163397448);
#1369=CONICAL_SURFACE('',#1665,1.9,0.785398163397448);
#1370=CONICAL_SURFACE('',#1669,1.1,0.785398163397448);
#1411=ADVANCED_FACE('',(#220,#119),#151,.F.);
#1412=ADVANCED_FACE('',(#221),#96,.F.);
#1413=ADVANCED_FACE('',(#222),#1367,.F.);
#1414=ADVANCED_FACE('',(#223),#97,.T.);
#1415=ADVANCED_FACE('',(#224,#120),#152,.T.);
#1416=ADVANCED_FACE('',(#225),#1368,.T.);
#1417=ADVANCED_FACE('',(#226,#121),#153,.F.);
#1418=ADVANCED_FACE('',(#227),#98,.T.);
#1419=ADVANCED_FACE('',(#228),#154,.T.);
#1420=ADVANCED_FACE('',(#229),#99,.T.);
#1421=ADVANCED_FACE('',(#230,#122),#155,.T.);
#1422=ADVANCED_FACE('',(#231),#100,.T.);
#1423=ADVANCED_FACE('',(#232),#1369,.T.);
#1424=ADVANCED_FACE('',(#233,#123),#156,.F.);
#1425=ADVANCED_FACE('',(#234),#1370,.F.);
#1426=ADVANCED_FACE('',(#235),#44,.F.);
#1479=CLOSED_SHELL('',(#1411,#1412,#1413,#1414,#1415,#1416));
#1480=CLOSED_SHELL('',(#1417,#1418,#1419,#1420,#1421,#1422,#1423,#1424,
#1425,#1426));
#1639=AXIS2_PLACEMENT_3D('',#2375,#1919,#1920);
#1640=AXIS2_PLACEMENT_3D('',#2376,#1921,#1922);
#1641=AXIS2_PLACEMENT_3D('',#2378,#1923,#1924);
#1642=AXIS2_PLACEMENT_3D('',#2380,#1925,#1926);
#1643=AXIS2_PLACEMENT_3D('',#2381,#1927,#1928);
#1644=AXIS2_PLACEMENT_3D('',#2383,#1929,#1930);
#1645=AXIS2_PLACEMENT_3D('',#2385,#1932,#1933);
#1646=AXIS2_PLACEMENT_3D('',#2388,#1935,#1936);
#1647=AXIS2_PLACEMENT_3D('',#2389,#1937,#1938);
#1648=AXIS2_PLACEMENT_3D('',#2392,#1940,#1941);
#1649=AXIS2_PLACEMENT_3D('',#2393,#1942,#1943);
#1650=AXIS2_PLACEMENT_3D('',#2395,#1944,#1945);
#1651=AXIS2_PLACEMENT_3D('',#2396,#1946,#1947);
#1652=AXIS2_PLACEMENT_3D('',#2398,#1949,#1950);
#1653=AXIS2_PLACEMENT_3D('',#2400,#1951,#1952);
#1654=AXIS2_PLACEMENT_3D('',#2402,#1953,#1954);
#1655=AXIS2_PLACEMENT_3D('',#2403,#1955,#1956);
#1656=AXIS2_PLACEMENT_3D('',#2406,#1958,#1959);
#1657=AXIS2_PLACEMENT_3D('',#2407,#1960,#1961);
#1658=AXIS2_PLACEMENT_3D('',#2409,#1962,#1963);
#1659=AXIS2_PLACEMENT_3D('',#2410,#1964,#1965);
#1660=AXIS2_PLACEMENT_3D('',#2412,#1966,#1967);
#1661=AXIS2_PLACEMENT_3D('',#2414,#1969,#1970);
#1662=AXIS2_PLACEMENT_3D('',#2416,#1971,#1972);
#1663=AXIS2_PLACEMENT_3D('',#2417,#1973,#1974);
#1664=AXIS2_PLACEMENT_3D('',#2419,#1975,#1976);
#1665=AXIS2_PLACEMENT_3D('',#2421,#1978,#1979);
#1666=AXIS2_PLACEMENT_3D('',#2424,#1981,#1982);
#1667=AXIS2_PLACEMENT_3D('',#2425,#1983,#1984);
#1668=AXIS2_PLACEMENT_3D('',#2427,#1985,#1986);
#1669=AXIS2_PLACEMENT_3D('',#2428,#1987,#1988);
#1670=AXIS2_PLACEMENT_3D('',#2430,#1990,#1991);
#1671=AXIS2_PLACEMENT_3D('',#2432,#1992,#1993);
#1919=DIRECTION('axis',(0.,0.,1.));
#1920=DIRECTION('refdir',(1.,0.,0.));
#1921=DIRECTION('center_axis',(0.,0.,1.));
#1922=DIRECTION('ref_axis',(-1.,0.,0.));
#1923=DIRECTION('center_axis',(0.,0.,-1.));
#1924=DIRECTION('ref_axis',(-1.,0.,0.));
#1925=DIRECTION('center_axis',(0.,0.,1.));
#1926=DIRECTION('ref_axis',(-1.,0.,0.));
#1927=DIRECTION('center_axis',(0.,0.,-1.));
#1928=DIRECTION('ref_axis',(-1.,0.,0.));
#1929=DIRECTION('center_axis',(0.,0.,-1.));
#1930=DIRECTION('ref_axis',(-1.,0.,0.));
#1931=DIRECTION('',(0.,0.,-1.));
#1932=DIRECTION('center_axis',(0.,0.,1.));
#1933=DIRECTION('ref_axis',(-1.,0.,0.));
#1934=DIRECTION('',(0.707106781186547,8.65956056235493E-17,0.707106781186548));
#1935=DIRECTION('center_axis',(0.,0.,1.));
#1936=DIRECTION('ref_axis',(-1.,0.,0.));
#1937=DIRECTION('center_axis',(0.,0.,-1.));
#1938=DIRECTION('ref_axis',(-1.,0.,0.));
#1939=DIRECTION('',(0.,0.,1.));
#1940=DIRECTION('center_axis',(0.,0.,1.));
#1941=DIRECTION('ref_axis',(-1.,0.,0.));
#1942=DIRECTION('center_axis',(0.,0.,1.));
#1943=DIRECTION('ref_axis',(-1.,0.,0.));
#1944=DIRECTION('center_axis',(0.,0.,-1.));
#1945=DIRECTION('ref_axis',(-1.,0.,0.));
#1946=DIRECTION('center_axis',(0.,0.,-1.));
#1947=DIRECTION('ref_axis',(-1.,0.,0.));
#1948=DIRECTION('',(-0.707106781186547,8.65956056235493E-17,0.707106781186548));
#1949=DIRECTION('center_axis',(0.,0.,1.));
#1950=DIRECTION('ref_axis',(-1.,0.,0.));
#1951=DIRECTION('center_axis',(0.,0.,-1.));
#1952=DIRECTION('ref_axis',(-1.,0.,0.));
#1953=DIRECTION('center_axis',(0.,0.,1.));
#1954=DIRECTION('ref_axis',(0.,-1.,0.));
#1955=DIRECTION('center_axis',(0.,0.,-1.));
#1956=DIRECTION('ref_axis',(-1.,0.,0.));
#1957=DIRECTION('',(0.,0.,1.));
#1958=DIRECTION('center_axis',(0.,0.,-1.));
#1959=DIRECTION('ref_axis',(-1.,0.,0.));
#1960=DIRECTION('center_axis',(0.,0.,1.));
#1961=DIRECTION('ref_axis',(-1.,0.,0.));
#1962=DIRECTION('center_axis',(0.,0.,1.));
#1963=DIRECTION('ref_axis',(-1.,0.,0.));
#1964=DIRECTION('center_axis',(0.,0.,-1.));
#1965=DIRECTION('ref_axis',(-1.,0.,0.));
#1966=DIRECTION('center_axis',(0.,0.,1.));
#1967=DIRECTION('ref_axis',(-1.,0.,0.));
#1968=DIRECTION('',(0.,0.,1.));
#1969=DIRECTION('center_axis',(0.,0.,1.));
#1970=DIRECTION('ref_axis',(-1.,0.,0.));
#1971=DIRECTION('center_axis',(0.,0.,-1.));
#1972=DIRECTION('ref_axis',(-1.,0.,0.));
#1973=DIRECTION('center_axis',(0.,0.,-1.));
#1974=DIRECTION('ref_axis',(-1.,0.,0.));
#1975=DIRECTION('center_axis',(0.,0.,-1.));
#1976=DIRECTION('ref_axis',(-1.,0.,0.));
#1977=DIRECTION('',(0.,0.,1.));
#1978=DIRECTION('center_axis',(0.,0.,1.));
#1979=DIRECTION('ref_axis',(-1.,0.,0.));
#1980=DIRECTION('',(-0.707106781186547,-8.65956056235493E-17,-0.707106781186548));
#1981=DIRECTION('center_axis',(0.,0.,1.));
#1982=DIRECTION('ref_axis',(-1.,0.,0.));
#1983=DIRECTION('center_axis',(0.,0.,1.));
#1984=DIRECTION('ref_axis',(-1.,0.,0.));
#1985=DIRECTION('center_axis',(0.,0.,-1.));
#1986=DIRECTION('ref_axis',(-1.,0.,0.));
#1987=DIRECTION('center_axis',(0.,0.,-1.));
#1988=DIRECTION('ref_axis',(-1.,0.,0.));
#1989=DIRECTION('',(0.707106781186547,-8.65956056235493E-17,-0.707106781186548));
#1990=DIRECTION('center_axis',(0.,0.,1.));
#1991=DIRECTION('ref_axis',(1.,0.,0.));
#1992=DIRECTION('center_axis',(0.,1.,0.));
#1993=DIRECTION('ref_axis',(-1.,0.,0.));
#2375=CARTESIAN_POINT('',(0.,0.,0.));
#2376=CARTESIAN_POINT('Origin',(8.,7.5,10.5));
#2377=CARTESIAN_POINT('',(10.,7.5,10.5));
#2378=CARTESIAN_POINT('Origin',(8.,7.5,10.5));
#2379=CARTESIAN_POINT('',(9.,7.5,10.5));
#2380=CARTESIAN_POINT('Origin',(8.,7.5,10.5));
#2381=CARTESIAN_POINT('Origin',(8.,7.5,12.5));
#2382=CARTESIAN_POINT('',(9.,7.5,12.3));
#2383=CARTESIAN_POINT('Origin',(8.,7.5,12.3));
#2384=CARTESIAN_POINT('',(9.,7.5,12.5));
#2385=CARTESIAN_POINT('Origin',(8.,7.5,12.4));
#2386=CARTESIAN_POINT('',(9.2,7.5,12.5));
#2387=CARTESIAN_POINT('',(9.1,7.5,12.4));
#2388=CARTESIAN_POINT('Origin',(8.,7.5,12.5));
#2389=CARTESIAN_POINT('Origin',(8.,7.5,12.5));
#2390=CARTESIAN_POINT('',(10.,7.5,12.3));
#2391=CARTESIAN_POINT('',(10.,7.5,12.5));
#2392=CARTESIAN_POINT('Origin',(8.,7.5,12.3));
#2393=CARTESIAN_POINT('Origin',(8.,7.5,12.5));
#2394=CARTESIAN_POINT('',(9.8,7.5,12.5));
#2395=CARTESIAN_POINT('Origin',(8.,7.5,12.5));
#2396=CARTESIAN_POINT('Origin',(8.,7.5,12.4));
#2397=CARTESIAN_POINT('',(9.9,7.5,12.4));
#2398=CARTESIAN_POINT('Origin',(8.,7.5,4.5));
#2399=CARTESIAN_POINT('',(9.,7.5,4.5));
#2400=CARTESIAN_POINT('Origin',(8.,7.5,4.5));
#2401=CARTESIAN_POINT('',(7.13397459621556,7.5,4.5));
#2402=CARTESIAN_POINT('Origin',(8.,7.5,4.5));
#2403=CARTESIAN_POINT('Origin',(8.,7.5,12.5));
#2404=CARTESIAN_POINT('',(9.,7.5,6.7));
#2405=CARTESIAN_POINT('',(9.,7.5,12.5));
#2406=CARTESIAN_POINT('Origin',(8.,7.5,6.7));
#2407=CARTESIAN_POINT('Origin',(8.,7.5,10.5));
#2408=CARTESIAN_POINT('',(9.,7.5,10.5));
#2409=CARTESIAN_POINT('Origin',(8.,7.5,10.5));
#2410=CARTESIAN_POINT('Origin',(8.,7.5,12.5));
#2411=CARTESIAN_POINT('',(9.,7.5,7.5));
#2412=CARTESIAN_POINT('Origin',(8.,7.5,7.5));
#2413=CARTESIAN_POINT('',(9.,7.5,12.5));
#2414=CARTESIAN_POINT('Origin',(8.,7.5,7.5));
#2415=CARTESIAN_POINT('',(10.,7.5,7.5));
#2416=CARTESIAN_POINT('Origin',(8.,7.5,7.5));
#2417=CARTESIAN_POINT('Origin',(8.,7.5,12.5));
#2418=CARTESIAN_POINT('',(10.,7.5,6.7));
#2419=CARTESIAN_POINT('Origin',(8.,7.5,6.7));
#2420=CARTESIAN_POINT('',(10.,7.5,12.5));
#2421=CARTESIAN_POINT('Origin',(8.,7.5,6.6));
#2422=CARTESIAN_POINT('',(9.8,7.5,6.5));
#2423=CARTESIAN_POINT('',(9.9,7.5,6.6));
#2424=CARTESIAN_POINT('Origin',(8.,7.5,6.5));
#2425=CARTESIAN_POINT('Origin',(8.,7.5,6.5));
#2426=CARTESIAN_POINT('',(9.2,7.5,6.5));
#2427=CARTESIAN_POINT('Origin',(8.,7.5,6.5));
#2428=CARTESIAN_POINT('Origin',(8.,7.5,6.6));
#2429=CARTESIAN_POINT('',(9.1,7.5,6.6));
#2430=CARTESIAN_POINT('Origin',(8.,7.5,4.));
#2431=CARTESIAN_POINT('',(8.,7.5,5.));
#2432=CARTESIAN_POINT('Origin',(8.,7.5,4.));
#2660=UNCERTAINTY_MEASURE_WITH_UNIT(LENGTH_MEASURE(0.01),#2677,
'DISTANCE_ACCURACY_VALUE',
'Maximum model space distance between geometric entities at asserted c
onnectivities');
#2666=UNCERTAINTY_MEASURE_WITH_UNIT(LENGTH_MEASURE(0.01),#2677,
'DISTANCE_ACCURACY_VALUE',
'Maximum model space distance between geometric entities at asserted c
onnectivities');
#2670=(
GEOMETRIC_REPRESENTATION_CONTEXT(3)
GLOBAL_UNCERTAINTY_ASSIGNED_CONTEXT((#2660))
GLOBAL_UNIT_ASSIGNED_CONTEXT((#2677,#2679,#2680))
REPRESENTATION_CONTEXT('','3D')
);
#2676=(
GEOMETRIC_REPRESENTATION_CONTEXT(3)
GLOBAL_UNCERTAINTY_ASSIGNED_CONTEXT((#2666))
GLOBAL_UNIT_ASSIGNED_CONTEXT((#2677,#2679,#2680))
REPRESENTATION_CONTEXT('','3D')
);
#2677=(
LENGTH_UNIT()
NAMED_UNIT(*)
SI_UNIT(.MILLI.,.METRE.)
);
#2679=(
NAMED_UNIT(*)
PLANE_ANGLE_UNIT()
SI_UNIT($,.RADIAN.)
);
#2680=(
NAMED_UNIT(*)
SI_UNIT($,.STERADIAN.)
SOLID_ANGLE_UNIT()
);
#2684=SHAPE_DEFINITION_REPRESENTATION(#2693,#2710);
#2693=PRODUCT_DEFINITION_SHAPE('',$,#2720);
#2710=SHAPE_REPRESENTATION('',(#1639),#2670);
#2716=PRODUCT_DEFINITION_CONTEXT('part definition',#2745,'design');
#2720=PRODUCT_DEFINITION('Screw_01','Screw_01',#2729,#2716);
#2729=PRODUCT_DEFINITION_FORMATION('',$,#2750);
#2745=APPLICATION_CONTEXT(
'Core Data for Automotive Mechanical Design Process');
#2746=PRODUCT_CONTEXT('part definition',#2745,'mechanical');
#2750=PRODUCT('Screw_01','Screw_01',$,(#2746));
#2757=PRESENTATION_STYLE_ASSIGNMENT((#2759));
#2759=SURFACE_STYLE_USAGE(.BOTH.,#2761);
#2761=SURFACE_SIDE_STYLE('',(#2763));
#2763=SURFACE_STYLE_FILL_AREA(#2765);
#2765=FILL_AREA_STYLE('Opaque(203,203,203)',(#2767));
#2767=FILL_AREA_STYLE_COLOUR('Opaque(203,203,203)',#2769);
#2769=COLOUR_RGB('Opaque(203,203,203)', 0.09019608, 0.27058824, 0.51372549);
ENDSEC;
END-ISO-10303-21;
